ISO-10303-21;
HEADER;
/* Generated by software containing ST-Developer
 * from STEP Tools, Inc. (www.steptools.com) 
 */

FILE_DESCRIPTION(
/* description */ (
'Independent keyed-quill tailstock, native coupled50mm slider andM16x2
 feed screw, conical dead center, bronze sleeves/thrust washers, cross
-pinned handwheel and bolted guide key. Custom center taper; no standa
rd taper compatibility, machine-bed compatibility or load rating assig
ned.'),
/* implementation_level */ '2;1');

FILE_NAME(
/* name */ 'Retaining pin washer.step',
/* time_stamp */ '2026-11-14T07:17:36-08:00',
/* author */ (''),
/* organization */ (''),
/* preprocessor_version */ 'ST-DEVELOPER v20.2',
/* originating_system */ 'Autodesk Translation Framework v15.17.0.0',
/* authorisation */ '');

FILE_SCHEMA (('AUTOMOTIVE_DESIGN { 1 0 10303 214 3 1 1 }'));
ENDSEC;

DATA;
#10=MECHANICAL_DESIGN_GEOMETRIC_PRESENTATION_REPRESENTATION('',(#164),#289387);
#130=SHAPE_REPRESENTATION_RELATIONSHIP('SRR','None',#289465,#147);
#147=ADVANCED_BREP_SHAPE_REPRESENTATION('',(#181),#289381);
#164=STYLED_ITEM('',(#289550),#181);
#181=MANIFOLD_SOLID_BREP('Body1',#16852);
#263=FACE_BOUND('',#1694,.T.);
#264=FACE_BOUND('',#1696,.T.);
#385=PLANE('',#17725);
#386=PLANE('',#17726);
#965=FACE_OUTER_BOUND('',#1691,.T.);
#966=FACE_OUTER_BOUND('',#1692,.T.);
#967=FACE_OUTER_BOUND('',#1693,.T.);
#968=FACE_OUTER_BOUND('',#1695,.T.);
#1691=EDGE_LOOP('',(#14797,#14798,#14799,#14800));
#1692=EDGE_LOOP('',(#14801,#14802,#14803,#14804));
#1693=EDGE_LOOP('',(#14805));
#1694=EDGE_LOOP('',(#14806));
#1695=EDGE_LOOP('',(#14807));
#1696=EDGE_LOOP('',(#14808));
#1951=CIRCLE('',#17720,2.);
#1952=CIRCLE('',#17721,2.);
#1953=CIRCLE('',#17723,3.5);
#1954=CIRCLE('',#17724,3.5);
#4460=LINE('',#247296,#5097);
#4461=LINE('',#247302,#5098);
#5097=VECTOR('',#19758,2.);
#5098=VECTOR('',#19765,3.5);
#7031=VERTEX_POINT('',#247293);
#7032=VERTEX_POINT('',#247295);
#7033=VERTEX_POINT('',#247299);
#7034=VERTEX_POINT('',#247301);
#9710=EDGE_CURVE('',#7031,#7031,#1951,.T.);
#9711=EDGE_CURVE('',#7031,#7032,#4460,.T.);
#9712=EDGE_CURVE('',#7032,#7032,#1952,.T.);
#9713=EDGE_CURVE('',#7033,#7033,#1953,.T.);
#9714=EDGE_CURVE('',#7033,#7034,#4461,.T.);
#9715=EDGE_CURVE('',#7034,#7034,#1954,.T.);
#14797=ORIENTED_EDGE('',*,*,#9710,.T.);
#14798=ORIENTED_EDGE('',*,*,#9711,.T.);
#14799=ORIENTED_EDGE('',*,*,#9712,.F.);
#14800=ORIENTED_EDGE('',*,*,#9711,.F.);
#14801=ORIENTED_EDGE('',*,*,#9713,.F.);
#14802=ORIENTED_EDGE('',*,*,#9714,.T.);
#14803=ORIENTED_EDGE('',*,*,#9715,.T.);
#14804=ORIENTED_EDGE('',*,*,#9714,.F.);
#14805=ORIENTED_EDGE('',*,*,#9713,.T.);
#14806=ORIENTED_EDGE('',*,*,#9712,.T.);
#14807=ORIENTED_EDGE('',*,*,#9715,.F.);
#14808=ORIENTED_EDGE('',*,*,#9710,.F.);
#16132=CYLINDRICAL_SURFACE('',#17719,2.);
#16133=CYLINDRICAL_SURFACE('',#17722,3.5);
#16733=ADVANCED_FACE('',(#965),#16132,.F.);
#16734=ADVANCED_FACE('',(#966),#16133,.T.);
#16735=ADVANCED_FACE('',(#967,#263),#385,.T.);
#16736=ADVANCED_FACE('',(#968,#264),#386,.F.);
#16852=CLOSED_SHELL('',(#16733,#16734,#16735,#16736));
#17718=AXIS2_PLACEMENT_3D('',#247291,#19752,#19753);
#17719=AXIS2_PLACEMENT_3D('',#247292,#19754,#19755);
#17720=AXIS2_PLACEMENT_3D('',#247294,#19756,#19757);
#17721=AXIS2_PLACEMENT_3D('',#247297,#19759,#19760);
#17722=AXIS2_PLACEMENT_3D('',#247298,#19761,#19762);
#17723=AXIS2_PLACEMENT_3D('',#247300,#19763,#19764);
#17724=AXIS2_PLACEMENT_3D('',#247303,#19766,#19767);
#17725=AXIS2_PLACEMENT_3D('',#247304,#19768,#19769);
#17726=AXIS2_PLACEMENT_3D('',#247305,#19770,#19771);
#19752=DIRECTION('axis',(0.,0.,1.));
#19753=DIRECTION('refdir',(1.,0.,0.));
#19754=DIRECTION('center_axis',(0.,0.,1.));
#19755=DIRECTION('ref_axis',(1.,0.,0.));
#19756=DIRECTION('center_axis',(0.,0.,-1.));
#19757=DIRECTION('ref_axis',(1.,0.,0.));
#19758=DIRECTION('',(0.,0.,1.));
#19759=DIRECTION('center_axis',(0.,0.,-1.));
#19760=DIRECTION('ref_axis',(1.,0.,0.));
#19761=DIRECTION('center_axis',(0.,0.,1.));
#19762=DIRECTION('ref_axis',(1.,0.,0.));
#19763=DIRECTION('center_axis',(0.,0.,1.));
#19764=DIRECTION('ref_axis',(1.,0.,0.));
#19765=DIRECTION('',(0.,0.,-1.));
#19766=DIRECTION('center_axis',(0.,0.,1.));
#19767=DIRECTION('ref_axis',(1.,0.,0.));
#19768=DIRECTION('center_axis',(0.,0.,1.));
#19769=DIRECTION('ref_axis',(1.,0.,0.));
#19770=DIRECTION('center_axis',(0.,0.,1.));
#19771=DIRECTION('ref_axis',(1.,0.,0.));
#247291=CARTESIAN_POINT('',(0.,0.,0.));
#247292=CARTESIAN_POINT('Origin',(0.,0.,0.));
#247293=CARTESIAN_POINT('',(-2.,-2.44929359829471E-16,0.));
#247294=CARTESIAN_POINT('Origin',(0.,0.,0.));
#247295=CARTESIAN_POINT('',(-2.,-2.44929359829471E-16,2.));
#247296=CARTESIAN_POINT('',(-2.,-2.44929359829471E-16,0.));
#247297=CARTESIAN_POINT('Origin',(0.,0.,2.));
#247298=CARTESIAN_POINT('Origin',(0.,0.,0.));
#247299=CARTESIAN_POINT('',(-3.5,-4.28626379701574E-16,2.));
#247300=CARTESIAN_POINT('Origin',(0.,0.,2.));
#247301=CARTESIAN_POINT('',(-3.5,-4.28626379701574E-16,0.));
#247302=CARTESIAN_POINT('',(-3.5,-4.28626379701574E-16,0.));
#247303=CARTESIAN_POINT('Origin',(0.,0.,0.));
#247304=CARTESIAN_POINT('Origin',(0.,0.,2.));
#247305=CARTESIAN_POINT('Origin',(0.,0.,0.));
#289362=UNCERTAINTY_MEASURE_WITH_UNIT(LENGTH_MEASURE(0.01),#289388,
'DISTANCE_ACCURACY_VALUE',
'Maximum model space distance between geometric entities at asserted c
onnectivities');
#289368=UNCERTAINTY_MEASURE_WITH_UNIT(LENGTH_MEASURE(0.01),#289388,
'DISTANCE_ACCURACY_VALUE',
'Maximum model space distance between geometric entities at asserted c
onnectivities');
#289381=(
GEOMETRIC_REPRESENTATION_CONTEXT(3)
GLOBAL_UNCERTAINTY_ASSIGNED_CONTEXT((#289362))
GLOBAL_UNIT_ASSIGNED_CONTEXT((#289388,#289390,#289391))
REPRESENTATION_CONTEXT('','3D')
);
#289387=(
GEOMETRIC_REPRESENTATION_CONTEXT(3)
GLOBAL_UNCERTAINTY_ASSIGNED_CONTEXT((#289368))
GLOBAL_UNIT_ASSIGNED_CONTEXT((#289388,#289390,#289391))
REPRESENTATION_CONTEXT('','3D')
);
#289388=(
LENGTH_UNIT()
NAMED_UNIT(*)
SI_UNIT(.MILLI.,.METRE.)
);
#289390=(
NAMED_UNIT(*)
PLANE_ANGLE_UNIT()
SI_UNIT($,.RADIAN.)
);
#289391=(
NAMED_UNIT(*)
SI_UNIT($,.STERADIAN.)
SOLID_ANGLE_UNIT()
);
#289404=SHAPE_DEFINITION_REPRESENTATION(#289422,#289465);
#289422=PRODUCT_DEFINITION_SHAPE('',$,#289484);
#289465=SHAPE_REPRESENTATION('',(#17718),#289381);
#289471=PRODUCT_DEFINITION_CONTEXT('part definition',#289527,'design');
#289484=PRODUCT_DEFINITION('Retaining pin washer',
'Retaining pin washer',#289502,#289471);
#289502=PRODUCT_DEFINITION_FORMATION('',$,#289541);
#289527=APPLICATION_CONTEXT(
'Core Data for Automotive Mechanical Design Process');
#289528=PRODUCT_CONTEXT('part definition',#289527,'mechanical');
#289541=PRODUCT('Retaining pin washer','Retaining pin washer',$,(#289528));
#289550=PRESENTATION_STYLE_ASSIGNMENT((#289557));
#289557=SURFACE_STYLE_USAGE(.BOTH.,#289564);
#289564=SURFACE_SIDE_STYLE('',(#289571));
#289571=SURFACE_STYLE_FILL_AREA(#289578);
#289578=FILL_AREA_STYLE('Opaque(185,192,202)',(#289585));
#289585=FILL_AREA_STYLE_COLOUR('Opaque(185,192,202)',#289592);
#289592=COLOUR_RGB('Opaque(185,192,202)',0.725490196078431,0.752941176470588,
0.792156862745098);
ENDSEC;
END-ISO-10303-21;
